ISO-10303-21;
HEADER;
/* Generated by software containing ST-Developer
 * from STEP Tools, Inc. (www.steptools.com) 
 */

FILE_DESCRIPTION(
/* description */ ('PAT-082'),
/* implementation_level */ '2;1');

FILE_NAME(
/* name */ 'Bonded pad.step',
/* time_stamp */ '2026-10-29T20:16:13-07:00',
/* author */ (''),
/* organization */ (''),
/* preprocessor_version */ 'ST-DEVELOPER v20.2',
/* originating_system */ 'Autodesk Translation Framework v15.17.0.0',
/* authorisation */ '');

FILE_SCHEMA (('AUTOMOTIVE_DESIGN { 1 0 10303 214 3 1 1 }'));
ENDSEC;

DATA;
#10=MECHANICAL_DESIGN_GEOMETRIC_PRESENTATION_REPRESENTATION('',(#242),#8266);
#198=SHAPE_REPRESENTATION_RELATIONSHIP('SRR','None',#8360,#220);
#220=ADVANCED_BREP_SHAPE_REPRESENTATION('',(#264),#8244);
#242=STYLED_ITEM('',(#8551),#264);
#264=MANIFOLD_SOLID_BREP('Body1',#4582);
#415=PLANE('',#4886);
#416=PLANE('',#4887);
#417=PLANE('',#4888);
#418=PLANE('',#4889);
#419=PLANE('',#4890);
#420=PLANE('',#4891);
#590=FACE_OUTER_BOUND('',#872,.T.);
#591=FACE_OUTER_BOUND('',#873,.T.);
#592=FACE_OUTER_BOUND('',#874,.T.);
#593=FACE_OUTER_BOUND('',#875,.T.);
#594=FACE_OUTER_BOUND('',#876,.T.);
#595=FACE_OUTER_BOUND('',#877,.T.);
#872=EDGE_LOOP('',(#3158,#3159,#3160,#3161));
#873=EDGE_LOOP('',(#3162,#3163,#3164,#3165));
#874=EDGE_LOOP('',(#3166,#3167,#3168,#3169));
#875=EDGE_LOOP('',(#3170,#3171,#3172,#3173));
#876=EDGE_LOOP('',(#3174,#3175,#3176,#3177));
#877=EDGE_LOOP('',(#3178,#3179,#3180,#3181));
#1255=LINE('',#6887,#1610);
#1256=LINE('',#6889,#1611);
#1257=LINE('',#6891,#1612);
#1258=LINE('',#6892,#1613);
#1259=LINE('',#6895,#1614);
#1260=LINE('',#6897,#1615);
#1261=LINE('',#6898,#1616);
#1262=LINE('',#6901,#1617);
#1263=LINE('',#6903,#1618);
#1264=LINE('',#6904,#1619);
#1265=LINE('',#6906,#1620);
#1266=LINE('',#6907,#1621);
#1610=VECTOR('',#5478,1.);
#1611=VECTOR('',#5479,1.);
#1612=VECTOR('',#5480,1.);
#1613=VECTOR('',#5481,1.);
#1614=VECTOR('',#5484,1.);
#1615=VECTOR('',#5485,1.);
#1616=VECTOR('',#5486,1.);
#1617=VECTOR('',#5489,1.);
#1618=VECTOR('',#5490,1.);
#1619=VECTOR('',#5491,1.);
#1620=VECTOR('',#5494,1.);
#1621=VECTOR('',#5495,1.);
#2169=VERTEX_POINT('',#6885);
#2170=VERTEX_POINT('',#6886);
#2171=VERTEX_POINT('',#6888);
#2172=VERTEX_POINT('',#6890);
#2173=VERTEX_POINT('',#6894);
#2174=VERTEX_POINT('',#6896);
#2175=VERTEX_POINT('',#6900);
#2176=VERTEX_POINT('',#6902);
#2555=EDGE_CURVE('',#2169,#2170,#1255,.T.);
#2556=EDGE_CURVE('',#2170,#2171,#1256,.T.);
#2557=EDGE_CURVE('',#2172,#2171,#1257,.T.);
#2558=EDGE_CURVE('',#2169,#2172,#1258,.T.);
#2559=EDGE_CURVE('',#2173,#2169,#1259,.T.);
#2560=EDGE_CURVE('',#2174,#2172,#1260,.T.);
#2561=EDGE_CURVE('',#2173,#2174,#1261,.T.);
#2562=EDGE_CURVE('',#2175,#2173,#1262,.T.);
#2563=EDGE_CURVE('',#2176,#2174,#1263,.T.);
#2564=EDGE_CURVE('',#2175,#2176,#1264,.T.);
#2565=EDGE_CURVE('',#2170,#2175,#1265,.T.);
#2566=EDGE_CURVE('',#2171,#2176,#1266,.T.);
#3158=ORIENTED_EDGE('',*,*,#2555,.T.);
#3159=ORIENTED_EDGE('',*,*,#2556,.T.);
#3160=ORIENTED_EDGE('',*,*,#2557,.F.);
#3161=ORIENTED_EDGE('',*,*,#2558,.F.);
#3162=ORIENTED_EDGE('',*,*,#2559,.T.);
#3163=ORIENTED_EDGE('',*,*,#2558,.T.);
#3164=ORIENTED_EDGE('',*,*,#2560,.F.);
#3165=ORIENTED_EDGE('',*,*,#2561,.F.);
#3166=ORIENTED_EDGE('',*,*,#2562,.T.);
#3167=ORIENTED_EDGE('',*,*,#2561,.T.);
#3168=ORIENTED_EDGE('',*,*,#2563,.F.);
#3169=ORIENTED_EDGE('',*,*,#2564,.F.);
#3170=ORIENTED_EDGE('',*,*,#2565,.T.);
#3171=ORIENTED_EDGE('',*,*,#2564,.T.);
#3172=ORIENTED_EDGE('',*,*,#2566,.F.);
#3173=ORIENTED_EDGE('',*,*,#2556,.F.);
#3174=ORIENTED_EDGE('',*,*,#2566,.T.);
#3175=ORIENTED_EDGE('',*,*,#2563,.T.);
#3176=ORIENTED_EDGE('',*,*,#2560,.T.);
#3177=ORIENTED_EDGE('',*,*,#2557,.T.);
#3178=ORIENTED_EDGE('',*,*,#2565,.F.);
#3179=ORIENTED_EDGE('',*,*,#2555,.F.);
#3180=ORIENTED_EDGE('',*,*,#2559,.F.);
#3181=ORIENTED_EDGE('',*,*,#2562,.F.);
#4329=ADVANCED_FACE('',(#590),#415,.T.);
#4330=ADVANCED_FACE('',(#591),#416,.T.);
#4331=ADVANCED_FACE('',(#592),#417,.T.);
#4332=ADVANCED_FACE('',(#593),#418,.T.);
#4333=ADVANCED_FACE('',(#594),#419,.T.);
#4334=ADVANCED_FACE('',(#595),#420,.F.);
#4582=CLOSED_SHELL('',(#4329,#4330,#4331,#4332,#4333,#4334));
#4885=AXIS2_PLACEMENT_3D('',#6883,#5474,#5475);
#4886=AXIS2_PLACEMENT_3D('',#6884,#5476,#5477);
#4887=AXIS2_PLACEMENT_3D('',#6893,#5482,#5483);
#4888=AXIS2_PLACEMENT_3D('',#6899,#5487,#5488);
#4889=AXIS2_PLACEMENT_3D('',#6905,#5492,#5493);
#4890=AXIS2_PLACEMENT_3D('',#6908,#5496,#5497);
#4891=AXIS2_PLACEMENT_3D('',#6909,#5498,#5499);
#5474=DIRECTION('axis',(0.,0.,1.));
#5475=DIRECTION('refdir',(1.,0.,0.));
#5476=DIRECTION('center_axis',(0.,1.,0.));
#5477=DIRECTION('ref_axis',(-1.,0.,0.));
#5478=DIRECTION('',(-1.,0.,0.));
#5479=DIRECTION('',(0.,0.,1.));
#5480=DIRECTION('',(-1.,0.,0.));
#5481=DIRECTION('',(0.,0.,1.));
#5482=DIRECTION('center_axis',(1.,0.,0.));
#5483=DIRECTION('ref_axis',(0.,1.,0.));
#5484=DIRECTION('',(0.,1.,0.));
#5485=DIRECTION('',(0.,1.,0.));
#5486=DIRECTION('',(0.,0.,1.));
#5487=DIRECTION('center_axis',(0.,-1.,0.));
#5488=DIRECTION('ref_axis',(1.,0.,0.));
#5489=DIRECTION('',(1.,0.,0.));
#5490=DIRECTION('',(1.,0.,0.));
#5491=DIRECTION('',(0.,0.,1.));
#5492=DIRECTION('center_axis',(-1.,0.,0.));
#5493=DIRECTION('ref_axis',(0.,-1.,0.));
#5494=DIRECTION('',(0.,-1.,0.));
#5495=DIRECTION('',(0.,-1.,0.));
#5496=DIRECTION('center_axis',(0.,0.,1.));
#5497=DIRECTION('ref_axis',(1.,0.,0.));
#5498=DIRECTION('center_axis',(0.,0.,1.));
#5499=DIRECTION('ref_axis',(1.,0.,0.));
#6883=CARTESIAN_POINT('',(0.,0.,0.));
#6884=CARTESIAN_POINT('Origin',(-6.,5.,-0.7));
#6885=CARTESIAN_POINT('',(-6.,5.,-0.7));
#6886=CARTESIAN_POINT('',(-8.,5.,-0.7));
#6887=CARTESIAN_POINT('',(-6.,5.,-0.7));
#6888=CARTESIAN_POINT('',(-8.,5.,-0.4));
#6889=CARTESIAN_POINT('',(-8.,5.,-0.7));
#6890=CARTESIAN_POINT('',(-6.,5.,-0.4));
#6891=CARTESIAN_POINT('',(-6.,5.,-0.4));
#6892=CARTESIAN_POINT('',(-6.,5.,-0.7));
#6893=CARTESIAN_POINT('Origin',(-6.,-5.,-0.7));
#6894=CARTESIAN_POINT('',(-6.,-5.,-0.7));
#6895=CARTESIAN_POINT('',(-6.,-5.,-0.7));
#6896=CARTESIAN_POINT('',(-6.,-5.,-0.4));
#6897=CARTESIAN_POINT('',(-6.,-5.,-0.4));
#6898=CARTESIAN_POINT('',(-6.,-5.,-0.7));
#6899=CARTESIAN_POINT('Origin',(-8.,-5.,-0.7));
#6900=CARTESIAN_POINT('',(-8.,-5.,-0.7));
#6901=CARTESIAN_POINT('',(-8.,-5.,-0.7));
#6902=CARTESIAN_POINT('',(-8.,-5.,-0.4));
#6903=CARTESIAN_POINT('',(-8.,-5.,-0.4));
#6904=CARTESIAN_POINT('',(-8.,-5.,-0.7));
#6905=CARTESIAN_POINT('Origin',(-8.,5.,-0.7));
#6906=CARTESIAN_POINT('',(-8.,5.,-0.7));
#6907=CARTESIAN_POINT('',(-8.,5.,-0.4));
#6908=CARTESIAN_POINT('Origin',(-7.,0.,-0.4));
#6909=CARTESIAN_POINT('Origin',(-7.,0.,-0.7));
#8219=UNCERTAINTY_MEASURE_WITH_UNIT(LENGTH_MEASURE(0.001),#8267,
'DISTANCE_ACCURACY_VALUE',
'Maximum model space distance between geometric entities at asserted c
onnectivities');
#8241=UNCERTAINTY_MEASURE_WITH_UNIT(LENGTH_MEASURE(0.001),#8267,
'DISTANCE_ACCURACY_VALUE',
'Maximum model space distance between geometric entities at asserted c
onnectivities');
#8244=(
GEOMETRIC_REPRESENTATION_CONTEXT(3)
GLOBAL_UNCERTAINTY_ASSIGNED_CONTEXT((#8219))
GLOBAL_UNIT_ASSIGNED_CONTEXT((#8267,#8269,#8270))
REPRESENTATION_CONTEXT('','3D')
);
#8266=(
GEOMETRIC_REPRESENTATION_CONTEXT(3)
GLOBAL_UNCERTAINTY_ASSIGNED_CONTEXT((#8241))
GLOBAL_UNIT_ASSIGNED_CONTEXT((#8267,#8269,#8270))
REPRESENTATION_CONTEXT('','3D')
);
#8267=(
LENGTH_UNIT()
NAMED_UNIT(*)
SI_UNIT(.CENTI.,.METRE.)
);
#8269=(
NAMED_UNIT(*)
PLANE_ANGLE_UNIT()
SI_UNIT($,.RADIAN.)
);
#8270=(
NAMED_UNIT(*)
SI_UNIT($,.STERADIAN.)
SOLID_ANGLE_UNIT()
);
#8273=SHAPE_DEFINITION_REPRESENTATION(#8297,#8360);
#8297=PRODUCT_DEFINITION_SHAPE('',$,#8385);
#8360=SHAPE_REPRESENTATION('',(#4885),#8244);
#8382=PRODUCT_DEFINITION_CONTEXT('part definition',#8456,'design');
#8385=PRODUCT_DEFINITION('Bonded pad','Bonded pad',#8409,#8382);
#8409=PRODUCT_DEFINITION_FORMATION('',$,#8460);
#8456=APPLICATION_CONTEXT(
'Core Data for Automotive Mechanical Design Process');
#8457=PRODUCT_CONTEXT('part definition',#8456,'mechanical');
#8460=PRODUCT('Bonded pad','Bonded pad','Bonded pad',(#8457));
#8545=COLOUR_RGB('Off White',0.89,0.88,0.83);
#8546=FILL_AREA_STYLE_COLOUR('',#8545);
#8547=FILL_AREA_STYLE('',(#8546));
#8548=SURFACE_STYLE_FILL_AREA(#8547);
#8549=SURFACE_SIDE_STYLE('',(#8548));
#8550=SURFACE_STYLE_USAGE(.BOTH.,#8549);
#8551=PRESENTATION_STYLE_ASSIGNMENT((#8550));
ENDSEC;
END-ISO-10303-21;
